ISO-10303-21;
HEADER;
/* Generated by software containing ST-Developer
 * from STEP Tools, Inc. (www.steptools.com) 
 */

FILE_DESCRIPTION(
/* description */ ('STEP AP214'),
/* implementation_level */ '2;1');

FILE_NAME(
/* name */ 'Hex Bolt.step',
/* time_stamp */ '2026-11-14T06:10:26-08:00',
/* author */ (''),
/* organization */ (''),
/* preprocessor_version */ 'ST-DEVELOPER v20.2',
/* originating_system */ 'Autodesk Translation Framework v15.17.0.0',
/* authorisation */ '');

FILE_SCHEMA (('AUTOMOTIVE_DESIGN { 1 0 10303 214 3 1 1 }'));
ENDSEC;

DATA;
#10=MECHANICAL_DESIGN_GEOMETRIC_PRESENTATION_REPRESENTATION('',(#170),#10413);
#154=SHAPE_REPRESENTATION_RELATIONSHIP('SRR','None',#10459,#162);
#162=ADVANCED_BREP_SHAPE_REPRESENTATION('',(#178),#10411);
#170=STYLED_ITEM('',(#10502),#178);
#178=MANIFOLD_SOLID_BREP('Body1',#5305);
#216=FACE_BOUND('',#859,.T.);
#258=PLANE('',#6089);
#259=PLANE('',#6090);
#260=PLANE('',#6091);
#261=PLANE('',#6092);
#262=PLANE('',#6093);
#263=PLANE('',#6094);
#264=PLANE('',#6095);
#265=PLANE('',#6096);
#266=PLANE('',#6097);
#531=FACE_OUTER_BOUND('',#857,.T.);
#532=FACE_OUTER_BOUND('',#858,.T.);
#533=FACE_OUTER_BOUND('',#860,.T.);
#534=FACE_OUTER_BOUND('',#861,.T.);
#535=FACE_OUTER_BOUND('',#862,.T.);
#536=FACE_OUTER_BOUND('',#863,.T.);
#537=FACE_OUTER_BOUND('',#864,.T.);
#538=FACE_OUTER_BOUND('',#865,.T.);
#539=FACE_OUTER_BOUND('',#866,.T.);
#540=FACE_OUTER_BOUND('',#867,.T.);
#857=EDGE_LOOP('',(#4622,#4623,#4624,#4625));
#858=EDGE_LOOP('',(#4626,#4627,#4628,#4629,#4630,#4631));
#859=EDGE_LOOP('',(#4632));
#860=EDGE_LOOP('',(#4633,#4634,#4635,#4636));
#861=EDGE_LOOP('',(#4637,#4638,#4639,#4640));
#862=EDGE_LOOP('',(#4641,#4642,#4643,#4644));
#863=EDGE_LOOP('',(#4645,#4646,#4647,#4648));
#864=EDGE_LOOP('',(#4649,#4650,#4651,#4652));
#865=EDGE_LOOP('',(#4653,#4654,#4655,#4656));
#866=EDGE_LOOP('',(#4657,#4658,#4659,#4660,#4661,#4662));
#867=EDGE_LOOP('',(#4663));
#1144=LINE('',#9427,#1435);
#1145=LINE('',#9432,#1436);
#1146=LINE('',#9434,#1437);
#1147=LINE('',#9436,#1438);
#1148=LINE('',#9438,#1439);
#1149=LINE('',#9440,#1440);
#1150=LINE('',#9441,#1441);
#1151=LINE('',#9445,#1442);
#1152=LINE('',#9446,#1443);
#1153=LINE('',#9447,#1444);
#1154=LINE('',#9450,#1445);
#1155=LINE('',#9451,#1446);
#1156=LINE('',#9454,#1447);
#1157=LINE('',#9455,#1448);
#1158=LINE('',#9458,#1449);
#1159=LINE('',#9459,#1450);
#1160=LINE('',#9462,#1451);
#1161=LINE('',#9463,#1452);
#1162=LINE('',#9465,#1453);
#1435=VECTOR('',#7784,2.5);
#1436=VECTOR('',#7789,1000.);
#1437=VECTOR('',#7790,1000.);
#1438=VECTOR('',#7791,1000.);
#1439=VECTOR('',#7792,1000.);
#1440=VECTOR('',#7793,1000.);
#1441=VECTOR('',#7794,1000.);
#1442=VECTOR('',#7797,1000.);
#1443=VECTOR('',#7798,1000.);
#1444=VECTOR('',#7799,1000.);
#1445=VECTOR('',#7802,1000.);
#1446=VECTOR('',#7803,1000.);
#1447=VECTOR('',#7806,1000.);
#1448=VECTOR('',#7807,1000.);
#1449=VECTOR('',#7810,1000.);
#1450=VECTOR('',#7811,1000.);
#1451=VECTOR('',#7814,1000.);
#1452=VECTOR('',#7815,1000.);
#1453=VECTOR('',#7818,1000.);
#1902=CIRCLE('',#6087,2.5);
#1903=CIRCLE('',#6088,2.5);
#2379=VERTEX_POINT('',#9424);
#2380=VERTEX_POINT('',#9426);
#2381=VERTEX_POINT('',#9430);
#2382=VERTEX_POINT('',#9431);
#2383=VERTEX_POINT('',#9433);
#2384=VERTEX_POINT('',#9435);
#2385=VERTEX_POINT('',#9437);
#2386=VERTEX_POINT('',#9439);
#2387=VERTEX_POINT('',#9443);
#2388=VERTEX_POINT('',#9444);
#2389=VERTEX_POINT('',#9449);
#2390=VERTEX_POINT('',#9453);
#2391=VERTEX_POINT('',#9457);
#2392=VERTEX_POINT('',#9461);
#3136=EDGE_CURVE('',#2379,#2379,#1902,.T.);
#3137=EDGE_CURVE('',#2379,#2380,#1144,.T.);
#3138=EDGE_CURVE('',#2380,#2380,#1903,.T.);
#3139=EDGE_CURVE('',#2381,#2382,#1145,.T.);
#3140=EDGE_CURVE('',#2382,#2383,#1146,.T.);
#3141=EDGE_CURVE('',#2383,#2384,#1147,.T.);
#3142=EDGE_CURVE('',#2384,#2385,#1148,.T.);
#3143=EDGE_CURVE('',#2385,#2386,#1149,.T.);
#3144=EDGE_CURVE('',#2386,#2381,#1150,.T.);
#3145=EDGE_CURVE('',#2387,#2388,#1151,.T.);
#3146=EDGE_CURVE('',#2382,#2388,#1152,.T.);
#3147=EDGE_CURVE('',#2381,#2387,#1153,.T.);
#3148=EDGE_CURVE('',#2388,#2389,#1154,.T.);
#3149=EDGE_CURVE('',#2383,#2389,#1155,.T.);
#3150=EDGE_CURVE('',#2389,#2390,#1156,.T.);
#3151=EDGE_CURVE('',#2384,#2390,#1157,.T.);
#3152=EDGE_CURVE('',#2390,#2391,#1158,.T.);
#3153=EDGE_CURVE('',#2385,#2391,#1159,.T.);
#3154=EDGE_CURVE('',#2391,#2392,#1160,.T.);
#3155=EDGE_CURVE('',#2386,#2392,#1161,.T.);
#3156=EDGE_CURVE('',#2392,#2387,#1162,.T.);
#4622=ORIENTED_EDGE('',*,*,#3136,.T.);
#4623=ORIENTED_EDGE('',*,*,#3137,.T.);
#4624=ORIENTED_EDGE('',*,*,#3138,.F.);
#4625=ORIENTED_EDGE('',*,*,#3137,.F.);
#4626=ORIENTED_EDGE('',*,*,#3139,.T.);
#4627=ORIENTED_EDGE('',*,*,#3140,.T.);
#4628=ORIENTED_EDGE('',*,*,#3141,.T.);
#4629=ORIENTED_EDGE('',*,*,#3142,.T.);
#4630=ORIENTED_EDGE('',*,*,#3143,.T.);
#4631=ORIENTED_EDGE('',*,*,#3144,.T.);
#4632=ORIENTED_EDGE('',*,*,#3136,.F.);
#4633=ORIENTED_EDGE('',*,*,#3145,.T.);
#4634=ORIENTED_EDGE('',*,*,#3146,.F.);
#4635=ORIENTED_EDGE('',*,*,#3139,.F.);
#4636=ORIENTED_EDGE('',*,*,#3147,.T.);
#4637=ORIENTED_EDGE('',*,*,#3148,.T.);
#4638=ORIENTED_EDGE('',*,*,#3149,.F.);
#4639=ORIENTED_EDGE('',*,*,#3140,.F.);
#4640=ORIENTED_EDGE('',*,*,#3146,.T.);
#4641=ORIENTED_EDGE('',*,*,#3150,.T.);
#4642=ORIENTED_EDGE('',*,*,#3151,.F.);
#4643=ORIENTED_EDGE('',*,*,#3141,.F.);
#4644=ORIENTED_EDGE('',*,*,#3149,.T.);
#4645=ORIENTED_EDGE('',*,*,#3152,.T.);
#4646=ORIENTED_EDGE('',*,*,#3153,.F.);
#4647=ORIENTED_EDGE('',*,*,#3142,.F.);
#4648=ORIENTED_EDGE('',*,*,#3151,.T.);
#4649=ORIENTED_EDGE('',*,*,#3154,.T.);
#4650=ORIENTED_EDGE('',*,*,#3155,.F.);
#4651=ORIENTED_EDGE('',*,*,#3143,.F.);
#4652=ORIENTED_EDGE('',*,*,#3153,.T.);
#4653=ORIENTED_EDGE('',*,*,#3156,.T.);
#4654=ORIENTED_EDGE('',*,*,#3147,.F.);
#4655=ORIENTED_EDGE('',*,*,#3144,.F.);
#4656=ORIENTED_EDGE('',*,*,#3155,.T.);
#4657=ORIENTED_EDGE('',*,*,#3145,.F.);
#4658=ORIENTED_EDGE('',*,*,#3156,.F.);
#4659=ORIENTED_EDGE('',*,*,#3154,.F.);
#4660=ORIENTED_EDGE('',*,*,#3152,.F.);
#4661=ORIENTED_EDGE('',*,*,#3150,.F.);
#4662=ORIENTED_EDGE('',*,*,#3148,.F.);
#4663=ORIENTED_EDGE('',*,*,#3138,.T.);
#4999=CYLINDRICAL_SURFACE('',#6086,2.5);
#5265=ADVANCED_FACE('',(#531),#4999,.T.);
#5266=ADVANCED_FACE('',(#532,#216),#258,.T.);
#5267=ADVANCED_FACE('',(#533),#259,.F.);
#5268=ADVANCED_FACE('',(#534),#260,.F.);
#5269=ADVANCED_FACE('',(#535),#261,.F.);
#5270=ADVANCED_FACE('',(#536),#262,.F.);
#5271=ADVANCED_FACE('',(#537),#263,.F.);
#5272=ADVANCED_FACE('',(#538),#264,.F.);
#5273=ADVANCED_FACE('',(#539),#265,.F.);
#5274=ADVANCED_FACE('',(#540),#266,.T.);
#5305=CLOSED_SHELL('',(#5265,#5266,#5267,#5268,#5269,#5270,#5271,#5272,
#5273,#5274));
#6085=AXIS2_PLACEMENT_3D('',#9422,#7778,#7779);
#6086=AXIS2_PLACEMENT_3D('',#9423,#7780,#7781);
#6087=AXIS2_PLACEMENT_3D('',#9425,#7782,#7783);
#6088=AXIS2_PLACEMENT_3D('',#9428,#7785,#7786);
#6089=AXIS2_PLACEMENT_3D('',#9429,#7787,#7788);
#6090=AXIS2_PLACEMENT_3D('',#9442,#7795,#7796);
#6091=AXIS2_PLACEMENT_3D('',#9448,#7800,#7801);
#6092=AXIS2_PLACEMENT_3D('',#9452,#7804,#7805);
#6093=AXIS2_PLACEMENT_3D('',#9456,#7808,#7809);
#6094=AXIS2_PLACEMENT_3D('',#9460,#7812,#7813);
#6095=AXIS2_PLACEMENT_3D('',#9464,#7816,#7817);
#6096=AXIS2_PLACEMENT_3D('',#9466,#7819,#7820);
#6097=AXIS2_PLACEMENT_3D('',#9467,#7821,#7822);
#7778=DIRECTION('axis',(0.,0.,1.));
#7779=DIRECTION('refdir',(1.,0.,0.));
#7780=DIRECTION('center_axis',(0.,0.,-1.));
#7781=DIRECTION('ref_axis',(-1.,0.,0.));
#7782=DIRECTION('center_axis',(0.,0.,1.));
#7783=DIRECTION('ref_axis',(1.,0.,0.));
#7784=DIRECTION('',(0.,0.,1.));
#7785=DIRECTION('center_axis',(0.,0.,1.));
#7786=DIRECTION('ref_axis',(1.,0.,0.));
#7787=DIRECTION('center_axis',(0.,0.,1.));
#7788=DIRECTION('ref_axis',(1.,0.,0.));
#7789=DIRECTION('',(0.500000000000001,0.866025403784438,0.));
#7790=DIRECTION('',(-0.500000000000001,0.866025403784438,0.));
#7791=DIRECTION('',(-1.,0.,0.));
#7792=DIRECTION('',(-0.500000000000001,-0.866025403784438,0.));
#7793=DIRECTION('',(0.499999999999999,-0.866025403784439,0.));
#7794=DIRECTION('',(1.,2.00308613164953E-15,0.));
#7795=DIRECTION('center_axis',(-0.866025403784438,0.500000000000001,0.));
#7796=DIRECTION('ref_axis',(-0.500000000000001,-0.866025403784438,0.));
#7797=DIRECTION('',(0.500000000000001,0.866025403784438,0.));
#7798=DIRECTION('',(0.,0.,-1.));
#7799=DIRECTION('',(0.,0.,-1.));
#7800=DIRECTION('center_axis',(-0.866025403784438,-0.500000000000001,0.));
#7801=DIRECTION('ref_axis',(0.500000000000001,-0.866025403784438,0.));
#7802=DIRECTION('',(-0.500000000000001,0.866025403784438,0.));
#7803=DIRECTION('',(0.,0.,-1.));
#7804=DIRECTION('center_axis',(0.,-1.,0.));
#7805=DIRECTION('ref_axis',(0.,0.,-1.));
#7806=DIRECTION('',(-1.,0.,0.));
#7807=DIRECTION('',(0.,0.,-1.));
#7808=DIRECTION('center_axis',(0.866025403784438,-0.500000000000001,0.));
#7809=DIRECTION('ref_axis',(0.500000000000001,0.866025403784438,0.));
#7810=DIRECTION('',(-0.500000000000001,-0.866025403784438,0.));
#7811=DIRECTION('',(0.,0.,-1.));
#7812=DIRECTION('center_axis',(0.866025403784439,0.499999999999999,0.));
#7813=DIRECTION('ref_axis',(-0.499999999999999,0.866025403784439,0.));
#7814=DIRECTION('',(0.499999999999999,-0.866025403784439,0.));
#7815=DIRECTION('',(0.,0.,-1.));
#7816=DIRECTION('center_axis',(-2.00308613164953E-15,1.,0.));
#7817=DIRECTION('ref_axis',(-1.,-2.00308613164953E-15,0.));
#7818=DIRECTION('',(1.,2.00308613164953E-15,0.));
#7819=DIRECTION('center_axis',(0.,0.,1.));
#7820=DIRECTION('ref_axis',(1.,0.,0.));
#7821=DIRECTION('center_axis',(0.,0.,1.));
#7822=DIRECTION('ref_axis',(1.,0.,0.));
#9422=CARTESIAN_POINT('',(0.,0.,0.));
#9423=CARTESIAN_POINT('Origin',(0.,0.,22.));
#9424=CARTESIAN_POINT('',(2.5,-3.06161699786838E-16,2.));
#9425=CARTESIAN_POINT('Origin',(0.,0.,2.));
#9426=CARTESIAN_POINT('',(2.5,-3.06161699786838E-16,22.));
#9427=CARTESIAN_POINT('',(2.5,-3.06161699786838E-16,22.));
#9428=CARTESIAN_POINT('Origin',(0.,0.,22.));
#9429=CARTESIAN_POINT('Origin',(0.,0.,2.));
#9430=CARTESIAN_POINT('',(1.73205080756887,-3.00000000000004,2.));
#9431=CARTESIAN_POINT('',(3.46410161513777,-7.54101367678791E-15,2.));
#9432=CARTESIAN_POINT('',(1.73205080756887,-3.00000000000004,2.));
#9433=CARTESIAN_POINT('',(1.73205080756885,3.00000000000006,2.));
#9434=CARTESIAN_POINT('',(3.46410161513777,-7.54101367678791E-15,2.));
#9435=CARTESIAN_POINT('',(-1.73205080756889,3.00000000000006,2.));
#9436=CARTESIAN_POINT('',(1.73205080756885,3.00000000000006,2.));
#9437=CARTESIAN_POINT('',(-3.46410161513781,-6.50677102219972E-15,2.));
#9438=CARTESIAN_POINT('',(-1.73205080756889,3.00000000000006,2.));
#9439=CARTESIAN_POINT('',(-1.73205080756891,-3.00000000000004,2.));
#9440=CARTESIAN_POINT('',(-3.46410161513781,-6.50677102219972E-15,2.));
#9441=CARTESIAN_POINT('',(-1.73205080756891,-3.00000000000004,2.));
#9442=CARTESIAN_POINT('Origin',(1.73205080756887,-3.00000000000004,2.));
#9443=CARTESIAN_POINT('',(1.73205080756887,-3.00000000000004,0.));
#9444=CARTESIAN_POINT('',(3.46410161513777,-7.54101367678791E-15,0.));
#9445=CARTESIAN_POINT('',(1.73205080756887,-3.00000000000004,0.));
#9446=CARTESIAN_POINT('',(3.46410161513777,-7.54101367678791E-15,2.));
#9447=CARTESIAN_POINT('',(1.73205080756887,-3.00000000000004,2.));
#9448=CARTESIAN_POINT('Origin',(3.46410161513777,-7.54101367678791E-15,
2.));
#9449=CARTESIAN_POINT('',(1.73205080756885,3.00000000000006,0.));
#9450=CARTESIAN_POINT('',(3.46410161513777,-7.54101367678791E-15,0.));
#9451=CARTESIAN_POINT('',(1.73205080756885,3.00000000000006,2.));
#9452=CARTESIAN_POINT('Origin',(1.73205080756885,3.00000000000006,2.));
#9453=CARTESIAN_POINT('',(-1.73205080756889,3.00000000000006,0.));
#9454=CARTESIAN_POINT('',(1.73205080756885,3.00000000000006,0.));
#9455=CARTESIAN_POINT('',(-1.73205080756889,3.00000000000006,2.));
#9456=CARTESIAN_POINT('Origin',(-1.73205080756889,3.00000000000006,2.));
#9457=CARTESIAN_POINT('',(-3.46410161513781,-6.50677102219972E-15,0.));
#9458=CARTESIAN_POINT('',(-1.73205080756889,3.00000000000006,0.));
#9459=CARTESIAN_POINT('',(-3.46410161513781,-6.50677102219972E-15,2.));
#9460=CARTESIAN_POINT('Origin',(-3.46410161513781,-6.50677102219972E-15,
2.));
#9461=CARTESIAN_POINT('',(-1.73205080756891,-3.00000000000004,0.));
#9462=CARTESIAN_POINT('',(-3.46410161513781,-6.50677102219972E-15,0.));
#9463=CARTESIAN_POINT('',(-1.73205080756891,-3.00000000000004,2.));
#9464=CARTESIAN_POINT('Origin',(-1.73205080756891,-3.00000000000004,2.));
#9465=CARTESIAN_POINT('',(-1.73205080756891,-3.00000000000004,0.));
#9466=CARTESIAN_POINT('Origin',(0.,0.,0.));
#9467=CARTESIAN_POINT('Origin',(0.,0.,22.));
#10401=UNCERTAINTY_MEASURE_WITH_UNIT(LENGTH_MEASURE(0.01),#10414,
'DISTANCE_ACCURACY_VALUE',
'Maximum model space distance between geometric entities at asserted c
onnectivities');
#10403=UNCERTAINTY_MEASURE_WITH_UNIT(LENGTH_MEASURE(0.01),#10414,
'DISTANCE_ACCURACY_VALUE',
'Maximum model space distance between geometric entities at asserted c
onnectivities');
#10411=(
GEOMETRIC_REPRESENTATION_CONTEXT(3)
GLOBAL_UNCERTAINTY_ASSIGNED_CONTEXT((#10401))
GLOBAL_UNIT_ASSIGNED_CONTEXT((#10414,#10416,#10417))
REPRESENTATION_CONTEXT('','3D')
);
#10413=(
GEOMETRIC_REPRESENTATION_CONTEXT(3)
GLOBAL_UNCERTAINTY_ASSIGNED_CONTEXT((#10403))
GLOBAL_UNIT_ASSIGNED_CONTEXT((#10414,#10416,#10417))
REPRESENTATION_CONTEXT('','3D')
);
#10414=(
LENGTH_UNIT()
NAMED_UNIT(*)
SI_UNIT(.MILLI.,.METRE.)
);
#10416=(
NAMED_UNIT(*)
PLANE_ANGLE_UNIT()
SI_UNIT($,.RADIAN.)
);
#10417=(
NAMED_UNIT(*)
SI_UNIT($,.STERADIAN.)
SOLID_ANGLE_UNIT()
);
#10425=SHAPE_DEFINITION_REPRESENTATION(#10434,#10459);
#10434=PRODUCT_DEFINITION_SHAPE('',$,#10469);
#10459=SHAPE_REPRESENTATION('',(#6085),#10411);
#10461=PRODUCT_DEFINITION_CONTEXT('part definition',#10490,'design');
#10469=PRODUCT_DEFINITION('Hex Bolt','Hex Bolt',#10478,#10461);
#10478=PRODUCT_DEFINITION_FORMATION('',$,#10499);
#10490=APPLICATION_CONTEXT(
'Core Data for Automotive Mechanical Design Process');
#10491=PRODUCT_CONTEXT('part definition',#10490,'mechanical');
#10499=PRODUCT('Hex Bolt','Hex Bolt',$,(#10491));
#10502=PRESENTATION_STYLE_ASSIGNMENT((#10506));
#10506=SURFACE_STYLE_USAGE(.BOTH.,#10510);
#10510=SURFACE_SIDE_STYLE('',(#10514));
#10514=SURFACE_STYLE_FILL_AREA(#10518);
#10518=FILL_AREA_STYLE('Opaque(61,176,222)',(#10522));
#10522=FILL_AREA_STYLE_COLOUR('Opaque(61,176,222)',#10526);
#10526=COLOUR_RGB('Opaque(61,176,222)',0.23921568627451,0.690196078431373,
0.870588235294118);
ENDSEC;
END-ISO-10303-21;
